ISO-10303-21;
HEADER;
/* Generated by software containing ST-Developer
 * from STEP Tools, Inc. (www.steptools.com) 
 */

FILE_DESCRIPTION(
/* description */ ('Independent manual traversing gantry with native reusable aluminum pr
ofiles,180mm captured carriage travel, four bronze-bushed rollers, lin
ked ideal rolling motion, bonded acetal lateral guides, positive welde
d end stops and fully retained axle stacks. Editable native profile cu
t lengths220/400mm. Tool attachments viaM6 bridge-plate taps; mounted 
tool outside assembly. Welds, anchors, adhesives, fits, traction, load
/speed/structural/life ratings unassigned.'),
/* implementation_level */ '2;1');

FILE_NAME(
/* name */ 'Bearing thrust washer.step',
/* time_stamp */ '2026-11-09T20:04:38-08:00',
/* author */ (''),
/* organization */ (''),
/* preprocessor_version */ 'ST-DEVELOPER v20.2',
/* originating_system */ 'Autodesk Translation Framework v15.17.0.0',
/* authorisation */ '');

FILE_SCHEMA (('AUTOMOTIVE_DESIGN { 1 0 10303 214 3 1 1 }'));
ENDSEC;

DATA;
#10=MECHANICAL_DESIGN_GEOMETRIC_PRESENTATION_REPRESENTATION('',(#485),#13231);
#453=SHAPE_REPRESENTATION_RELATIONSHIP('SRR','None',#13342,#469);
#469=ADVANCED_BREP_SHAPE_REPRESENTATION('',(#501),#13229);
#485=STYLED_ITEM('',(#13429),#501);
#501=MANIFOLD_SOLID_BREP('Body1',#4165);
#548=FACE_BOUND('',#1115,.T.);
#549=FACE_BOUND('',#1117,.T.);
#629=PLANE('',#4667);
#630=PLANE('',#4668);
#846=FACE_OUTER_BOUND('',#1112,.T.);
#847=FACE_OUTER_BOUND('',#1113,.T.);
#848=FACE_OUTER_BOUND('',#1114,.T.);
#849=FACE_OUTER_BOUND('',#1116,.T.);
#1112=EDGE_LOOP('',(#3774,#3775,#3776,#3777));
#1113=EDGE_LOOP('',(#3778,#3779,#3780,#3781));
#1114=EDGE_LOOP('',(#3782));
#1115=EDGE_LOOP('',(#3783));
#1116=EDGE_LOOP('',(#3784));
#1117=EDGE_LOOP('',(#3785));
#1382=LINE('',#13114,#1644);
#1383=LINE('',#13120,#1645);
#1644=VECTOR('',#5631,6.);
#1645=VECTOR('',#5638,11.);
#1744=CIRCLE('',#4662,6.);
#1745=CIRCLE('',#4663,6.);
#1746=CIRCLE('',#4665,11.);
#1747=CIRCLE('',#4666,11.);
#2116=VERTEX_POINT('',#13111);
#2117=VERTEX_POINT('',#13113);
#2118=VERTEX_POINT('',#13117);
#2119=VERTEX_POINT('',#13119);
#2670=EDGE_CURVE('',#2116,#2116,#1744,.T.);
#2671=EDGE_CURVE('',#2116,#2117,#1382,.T.);
#2672=EDGE_CURVE('',#2117,#2117,#1745,.T.);
#2673=EDGE_CURVE('',#2118,#2118,#1746,.T.);
#2674=EDGE_CURVE('',#2118,#2119,#1383,.T.);
#2675=EDGE_CURVE('',#2119,#2119,#1747,.T.);
#3774=ORIENTED_EDGE('',*,*,#2670,.F.);
#3775=ORIENTED_EDGE('',*,*,#2671,.T.);
#3776=ORIENTED_EDGE('',*,*,#2672,.T.);
#3777=ORIENTED_EDGE('',*,*,#2671,.F.);
#3778=ORIENTED_EDGE('',*,*,#2673,.F.);
#3779=ORIENTED_EDGE('',*,*,#2674,.T.);
#3780=ORIENTED_EDGE('',*,*,#2675,.T.);
#3781=ORIENTED_EDGE('',*,*,#2674,.F.);
#3782=ORIENTED_EDGE('',*,*,#2673,.T.);
#3783=ORIENTED_EDGE('',*,*,#2670,.T.);
#3784=ORIENTED_EDGE('',*,*,#2675,.F.);
#3785=ORIENTED_EDGE('',*,*,#2672,.F.);
#3926=CYLINDRICAL_SURFACE('',#4661,6.);
#3927=CYLINDRICAL_SURFACE('',#4664,11.);
#4143=ADVANCED_FACE('',(#846),#3926,.F.);
#4144=ADVANCED_FACE('',(#847),#3927,.T.);
#4145=ADVANCED_FACE('',(#848,#548),#629,.T.);
#4146=ADVANCED_FACE('',(#849,#549),#630,.F.);
#4165=CLOSED_SHELL('',(#4143,#4144,#4145,#4146));
#4660=AXIS2_PLACEMENT_3D('',#13109,#5625,#5626);
#4661=AXIS2_PLACEMENT_3D('',#13110,#5627,#5628);
#4662=AXIS2_PLACEMENT_3D('',#13112,#5629,#5630);
#4663=AXIS2_PLACEMENT_3D('',#13115,#5632,#5633);
#4664=AXIS2_PLACEMENT_3D('',#13116,#5634,#5635);
#4665=AXIS2_PLACEMENT_3D('',#13118,#5636,#5637);
#4666=AXIS2_PLACEMENT_3D('',#13121,#5639,#5640);
#4667=AXIS2_PLACEMENT_3D('',#13122,#5641,#5642);
#4668=AXIS2_PLACEMENT_3D('',#13123,#5643,#5644);
#5625=DIRECTION('axis',(0.,0.,1.));
#5626=DIRECTION('refdir',(1.,0.,0.));
#5627=DIRECTION('center_axis',(0.,0.,1.));
#5628=DIRECTION('ref_axis',(1.,0.,0.));
#5629=DIRECTION('center_axis',(0.,0.,-1.));
#5630=DIRECTION('ref_axis',(1.,0.,0.));
#5631=DIRECTION('',(0.,0.,-1.));
#5632=DIRECTION('center_axis',(0.,0.,-1.));
#5633=DIRECTION('ref_axis',(1.,0.,0.));
#5634=DIRECTION('center_axis',(0.,0.,1.));
#5635=DIRECTION('ref_axis',(1.,0.,0.));
#5636=DIRECTION('center_axis',(0.,0.,1.));
#5637=DIRECTION('ref_axis',(1.,0.,0.));
#5638=DIRECTION('',(0.,0.,-1.));
#5639=DIRECTION('center_axis',(0.,0.,1.));
#5640=DIRECTION('ref_axis',(1.,0.,0.));
#5641=DIRECTION('center_axis',(0.,0.,1.));
#5642=DIRECTION('ref_axis',(1.,0.,0.));
#5643=DIRECTION('center_axis',(0.,0.,1.));
#5644=DIRECTION('ref_axis',(1.,0.,0.));
#13109=CARTESIAN_POINT('',(0.,0.,0.));
#13110=CARTESIAN_POINT('Origin',(0.,0.,0.));
#13111=CARTESIAN_POINT('',(-6.,-7.34788079488412E-16,1.));
#13112=CARTESIAN_POINT('Origin',(0.,0.,1.));
#13113=CARTESIAN_POINT('',(-6.,-7.34788079488412E-16,0.));
#13114=CARTESIAN_POINT('',(-6.,-7.34788079488412E-16,0.));
#13115=CARTESIAN_POINT('Origin',(0.,0.,0.));
#13116=CARTESIAN_POINT('Origin',(0.,0.,0.));
#13117=CARTESIAN_POINT('',(-11.,-1.34711147906209E-15,1.));
#13118=CARTESIAN_POINT('Origin',(0.,0.,1.));
#13119=CARTESIAN_POINT('',(-11.,-1.34711147906209E-15,0.));
#13120=CARTESIAN_POINT('',(-11.,-1.34711147906209E-15,0.));
#13121=CARTESIAN_POINT('Origin',(0.,0.,0.));
#13122=CARTESIAN_POINT('Origin',(0.,0.,1.));
#13123=CARTESIAN_POINT('Origin',(0.,0.,0.));
#13211=UNCERTAINTY_MEASURE_WITH_UNIT(LENGTH_MEASURE(0.01),#13232,
'DISTANCE_ACCURACY_VALUE',
'Maximum model space distance between geometric entities at asserted c
onnectivities');
#13213=UNCERTAINTY_MEASURE_WITH_UNIT(LENGTH_MEASURE(0.01),#13232,
'DISTANCE_ACCURACY_VALUE',
'Maximum model space distance between geometric entities at asserted c
onnectivities');
#13229=(
GEOMETRIC_REPRESENTATION_CONTEXT(3)
GLOBAL_UNCERTAINTY_ASSIGNED_CONTEXT((#13211))
GLOBAL_UNIT_ASSIGNED_CONTEXT((#13232,#13234,#13235))
REPRESENTATION_CONTEXT('','3D')
);
#13231=(
GEOMETRIC_REPRESENTATION_CONTEXT(3)
GLOBAL_UNCERTAINTY_ASSIGNED_CONTEXT((#13213))
GLOBAL_UNIT_ASSIGNED_CONTEXT((#13232,#13234,#13235))
REPRESENTATION_CONTEXT('','3D')
);
#13232=(
LENGTH_UNIT()
NAMED_UNIT(*)
SI_UNIT(.MILLI.,.METRE.)
);
#13234=(
NAMED_UNIT(*)
PLANE_ANGLE_UNIT()
SI_UNIT($,.RADIAN.)
);
#13235=(
NAMED_UNIT(*)
SI_UNIT($,.STERADIAN.)
SOLID_ANGLE_UNIT()
);
#13251=SHAPE_DEFINITION_REPRESENTATION(#13268,#13342);
#13268=PRODUCT_DEFINITION_SHAPE('',$,#13360);
#13342=SHAPE_REPRESENTATION('',(#4660),#13229);
#13344=PRODUCT_DEFINITION_CONTEXT('part definition',#13397,'design');
#13360=PRODUCT_DEFINITION('Bearing thrust washer',
'Bearing thrust washer',#13377,#13344);
#13377=PRODUCT_DEFINITION_FORMATION('',$,#13414);
#13397=APPLICATION_CONTEXT(
'Core Data for Automotive Mechanical Design Process');
#13398=PRODUCT_CONTEXT('part definition',#13397,'mechanical');
#13414=PRODUCT('Bearing thrust washer','Bearing thrust washer',$,(#13398));
#13429=PRESENTATION_STYLE_ASSIGNMENT((#13443));
#13443=SURFACE_STYLE_USAGE(.BOTH.,#13457);
#13457=SURFACE_SIDE_STYLE('',(#13471));
#13471=SURFACE_STYLE_FILL_AREA(#13485);
#13485=FILL_AREA_STYLE('Bearing light gray',(#13499));
#13499=FILL_AREA_STYLE_COLOUR('Bearing light gray',#13513);
#13513=COLOUR_RGB('Bearing light gray',0.725490196078431,0.752941176470588,
0.792156862745098);
ENDSEC;
END-ISO-10303-21;
